ISO-10303-21;
HEADER;
/* Generated by software containing ST-Developer
 * from STEP Tools, Inc. (www.steptools.com) 
 */

FILE_DESCRIPTION(
/* description */ (''),
/* implementation_level */ '2;1');

FILE_NAME(
/* name */ '07_Needle_Bearing_HK1716_Drawn_Cup.step',
/* time_stamp */ '2026-10-26T06:59:52-07:00',
/* author */ (''),
/* organization */ (''),
/* preprocessor_version */ 'ST-DEVELOPER v20.2',
/* originating_system */ 'Autodesk Translation Framework v15.15.0.0',
/* authorisation */ '');

FILE_SCHEMA (('AUTOMOTIVE_DESIGN { 1 0 10303 214 3 1 1 }'));
ENDSEC;

DATA;
#10=MECHANICAL_DESIGN_GEOMETRIC_PRESENTATION_REPRESENTATION('',(#175),#46395);
#147=SHAPE_REPRESENTATION_RELATIONSHIP('SRR','None',#46467,#161);
#161=ADVANCED_BREP_SHAPE_REPRESENTATION('',(#189),#46392);
#175=STYLED_ITEM('',(#46596),#189);
#189=MANIFOLD_SOLID_BREP('Body1',#24948);
#534=CYLINDRICAL_SURFACE('',#26581,8.5);
#535=CYLINDRICAL_SURFACE('',#26588,10.7);
#536=CYLINDRICAL_SURFACE('',#26590,9.);
#537=CYLINDRICAL_SURFACE('',#26595,11.5);
#538=CYLINDRICAL_SURFACE('',#26599,9.);
#539=CYLINDRICAL_SURFACE('',#26602,10.7);
#668=FACE_BOUND('',#4270,.T.);
#669=FACE_BOUND('',#4272,.T.);
#670=FACE_BOUND('',#4276,.T.);
#671=FACE_BOUND('',#4279,.T.);
#672=FACE_BOUND('',#4282,.T.);
#673=FACE_BOUND('',#4285,.T.);
#1583=PLANE('',#26584);
#1584=PLANE('',#26586);
#1585=PLANE('',#26593);
#1586=PLANE('',#26597);
#1587=PLANE('',#26601);
#1588=PLANE('',#26604);
#2855=FACE_OUTER_BOUND('',#4268,.T.);
#2856=FACE_OUTER_BOUND('',#4269,.T.);
#2857=FACE_OUTER_BOUND('',#4271,.T.);
#2858=FACE_OUTER_BOUND('',#4273,.T.);
#2859=FACE_OUTER_BOUND('',#4274,.T.);
#2860=FACE_OUTER_BOUND('',#4275,.T.);
#2861=FACE_OUTER_BOUND('',#4277,.T.);
#2862=FACE_OUTER_BOUND('',#4278,.T.);
#2863=FACE_OUTER_BOUND('',#4280,.T.);
#2864=FACE_OUTER_BOUND('',#4281,.T.);
#2865=FACE_OUTER_BOUND('',#4283,.T.);
#2866=FACE_OUTER_BOUND('',#4284,.T.);
#4268=EDGE_LOOP('',(#22512,#22513,#22514,#22515));
#4269=EDGE_LOOP('',(#22516));
#4270=EDGE_LOOP('',(#22517));
#4271=EDGE_LOOP('',(#22518));
#4272=EDGE_LOOP('',(#22519));
#4273=EDGE_LOOP('',(#22520,#22521,#22522,#22523));
#4274=EDGE_LOOP('',(#22524,#22525,#22526,#22527));
#4275=EDGE_LOOP('',(#22528));
#4276=EDGE_LOOP('',(#22529));
#4277=EDGE_LOOP('',(#22530,#22531,#22532,#22533));
#4278=EDGE_LOOP('',(#22534));
#4279=EDGE_LOOP('',(#22535));
#4280=EDGE_LOOP('',(#22536,#22537,#22538,#22539));
#4281=EDGE_LOOP('',(#22540));
#4282=EDGE_LOOP('',(#22541));
#4283=EDGE_LOOP('',(#22542,#22543,#22544,#22545));
#4284=EDGE_LOOP('',(#22546));
#4285=EDGE_LOOP('',(#22547));
#7077=LINE('',#40691,#9946);
#7078=LINE('',#40702,#9947);
#7079=LINE('',#40707,#9948);
#7080=LINE('',#40715,#9949);
#7081=LINE('',#40721,#9950);
#7082=LINE('',#40726,#9951);
#9946=VECTOR('',#32430,8.5);
#9947=VECTOR('',#32445,10.7);
#9948=VECTOR('',#32450,9.);
#9949=VECTOR('',#32461,11.5);
#9950=VECTOR('',#32468,9.);
#9951=VECTOR('',#32475,10.7);
#10630=CIRCLE('',#26582,8.5);
#10631=CIRCLE('',#26583,8.5);
#10632=CIRCLE('',#26585,10.7);
#10633=CIRCLE('',#26587,10.7);
#10634=CIRCLE('',#26589,10.7);
#10635=CIRCLE('',#26591,9.);
#10636=CIRCLE('',#26592,9.);
#10637=CIRCLE('',#26594,11.5);
#10638=CIRCLE('',#26596,11.5);
#10639=CIRCLE('',#26598,9.);
#10640=CIRCLE('',#26600,9.);
#10641=CIRCLE('',#26603,10.7);
#12674=VERTEX_POINT('',#40688);
#12675=VERTEX_POINT('',#40690);
#12676=VERTEX_POINT('',#40694);
#12677=VERTEX_POINT('',#40697);
#12678=VERTEX_POINT('',#40700);
#12679=VERTEX_POINT('',#40704);
#12680=VERTEX_POINT('',#40706);
#12681=VERTEX_POINT('',#40710);
#12682=VERTEX_POINT('',#40713);
#12683=VERTEX_POINT('',#40717);
#12684=VERTEX_POINT('',#40720);
#12685=VERTEX_POINT('',#40725);
#16009=EDGE_CURVE('',#12674,#12674,#10630,.T.);
#16010=EDGE_CURVE('',#12674,#12675,#7077,.T.);
#16011=EDGE_CURVE('',#12675,#12675,#10631,.T.);
#16012=EDGE_CURVE('',#12676,#12676,#10632,.T.);
#16013=EDGE_CURVE('',#12677,#12677,#10633,.T.);
#16014=EDGE_CURVE('',#12678,#12678,#10634,.T.);
#16015=EDGE_CURVE('',#12678,#12677,#7078,.T.);
#16016=EDGE_CURVE('',#12679,#12679,#10635,.T.);
#16017=EDGE_CURVE('',#12679,#12680,#7079,.T.);
#16018=EDGE_CURVE('',#12680,#12680,#10636,.T.);
#16019=EDGE_CURVE('',#12681,#12681,#10637,.T.);
#16020=EDGE_CURVE('',#12682,#12682,#10638,.T.);
#16021=EDGE_CURVE('',#12682,#12681,#7080,.T.);
#16022=EDGE_CURVE('',#12683,#12683,#10639,.T.);
#16023=EDGE_CURVE('',#12683,#12684,#7081,.T.);
#16024=EDGE_CURVE('',#12684,#12684,#10640,.T.);
#16025=EDGE_CURVE('',#12676,#12685,#7082,.T.);
#16026=EDGE_CURVE('',#12685,#12685,#10641,.T.);
#22512=ORIENTED_EDGE('',*,*,#16009,.T.);
#22513=ORIENTED_EDGE('',*,*,#16010,.T.);
#22514=ORIENTED_EDGE('',*,*,#16011,.F.);
#22515=ORIENTED_EDGE('',*,*,#16010,.F.);
#22516=ORIENTED_EDGE('',*,*,#16012,.F.);
#22517=ORIENTED_EDGE('',*,*,#16011,.T.);
#22518=ORIENTED_EDGE('',*,*,#16013,.F.);
#22519=ORIENTED_EDGE('',*,*,#16009,.F.);
#22520=ORIENTED_EDGE('',*,*,#16014,.T.);
#22521=ORIENTED_EDGE('',*,*,#16015,.T.);
#22522=ORIENTED_EDGE('',*,*,#16013,.T.);
#22523=ORIENTED_EDGE('',*,*,#16015,.F.);
#22524=ORIENTED_EDGE('',*,*,#16016,.T.);
#22525=ORIENTED_EDGE('',*,*,#16017,.T.);
#22526=ORIENTED_EDGE('',*,*,#16018,.F.);
#22527=ORIENTED_EDGE('',*,*,#16017,.F.);
#22528=ORIENTED_EDGE('',*,*,#16019,.F.);
#22529=ORIENTED_EDGE('',*,*,#16018,.T.);
#22530=ORIENTED_EDGE('',*,*,#16020,.F.);
#22531=ORIENTED_EDGE('',*,*,#16021,.T.);
#22532=ORIENTED_EDGE('',*,*,#16019,.T.);
#22533=ORIENTED_EDGE('',*,*,#16021,.F.);
#22534=ORIENTED_EDGE('',*,*,#16020,.T.);
#22535=ORIENTED_EDGE('',*,*,#16022,.F.);
#22536=ORIENTED_EDGE('',*,*,#16022,.T.);
#22537=ORIENTED_EDGE('',*,*,#16023,.T.);
#22538=ORIENTED_EDGE('',*,*,#16024,.F.);
#22539=ORIENTED_EDGE('',*,*,#16023,.F.);
#22540=ORIENTED_EDGE('',*,*,#16014,.F.);
#22541=ORIENTED_EDGE('',*,*,#16024,.T.);
#22542=ORIENTED_EDGE('',*,*,#16012,.T.);
#22543=ORIENTED_EDGE('',*,*,#16025,.T.);
#22544=ORIENTED_EDGE('',*,*,#16026,.F.);
#22545=ORIENTED_EDGE('',*,*,#16025,.F.);
#22546=ORIENTED_EDGE('',*,*,#16026,.T.);
#22547=ORIENTED_EDGE('',*,*,#16016,.F.);
#24714=ADVANCED_FACE('',(#2855),#534,.F.);
#24715=ADVANCED_FACE('',(#2856,#668),#1583,.T.);
#24716=ADVANCED_FACE('',(#2857,#669),#1584,.T.);
#24717=ADVANCED_FACE('',(#2858),#535,.F.);
#24718=ADVANCED_FACE('',(#2859),#536,.F.);
#24719=ADVANCED_FACE('',(#2860,#670),#1585,.T.);
#24720=ADVANCED_FACE('',(#2861),#537,.T.);
#24721=ADVANCED_FACE('',(#2862,#671),#1586,.T.);
#24722=ADVANCED_FACE('',(#2863),#538,.F.);
#24723=ADVANCED_FACE('',(#2864,#672),#1587,.T.);
#24724=ADVANCED_FACE('',(#2865),#539,.F.);
#24725=ADVANCED_FACE('',(#2866,#673),#1588,.T.);
#24948=CLOSED_SHELL('',(#24714,#24715,#24716,#24717,#24718,#24719,#24720,
#24721,#24722,#24723,#24724,#24725));
#26580=AXIS2_PLACEMENT_3D('',#40686,#32424,#32425);
#26581=AXIS2_PLACEMENT_3D('',#40687,#32426,#32427);
#26582=AXIS2_PLACEMENT_3D('',#40689,#32428,#32429);
#26583=AXIS2_PLACEMENT_3D('',#40692,#32431,#32432);
#26584=AXIS2_PLACEMENT_3D('',#40693,#32433,#32434);
#26585=AXIS2_PLACEMENT_3D('',#40695,#32435,#32436);
#26586=AXIS2_PLACEMENT_3D('',#40696,#32437,#32438);
#26587=AXIS2_PLACEMENT_3D('',#40698,#32439,#32440);
#26588=AXIS2_PLACEMENT_3D('',#40699,#32441,#32442);
#26589=AXIS2_PLACEMENT_3D('',#40701,#32443,#32444);
#26590=AXIS2_PLACEMENT_3D('',#40703,#32446,#32447);
#26591=AXIS2_PLACEMENT_3D('',#40705,#32448,#32449);
#26592=AXIS2_PLACEMENT_3D('',#40708,#32451,#32452);
#26593=AXIS2_PLACEMENT_3D('',#40709,#32453,#32454);
#26594=AXIS2_PLACEMENT_3D('',#40711,#32455,#32456);
#26595=AXIS2_PLACEMENT_3D('',#40712,#32457,#32458);
#26596=AXIS2_PLACEMENT_3D('',#40714,#32459,#32460);
#26597=AXIS2_PLACEMENT_3D('',#40716,#32462,#32463);
#26598=AXIS2_PLACEMENT_3D('',#40718,#32464,#32465);
#26599=AXIS2_PLACEMENT_3D('',#40719,#32466,#32467);
#26600=AXIS2_PLACEMENT_3D('',#40722,#32469,#32470);
#26601=AXIS2_PLACEMENT_3D('',#40723,#32471,#32472);
#26602=AXIS2_PLACEMENT_3D('',#40724,#32473,#32474);
#26603=AXIS2_PLACEMENT_3D('',#40727,#32476,#32477);
#26604=AXIS2_PLACEMENT_3D('',#40728,#32478,#32479);
#32424=DIRECTION('axis',(0.,0.,1.));
#32425=DIRECTION('refdir',(1.,0.,0.));
#32426=DIRECTION('center_axis',(1.,0.,0.));
#32427=DIRECTION('ref_axis',(0.,1.,0.));
#32428=DIRECTION('center_axis',(1.,0.,0.));
#32429=DIRECTION('ref_axis',(0.,0.,-1.));
#32430=DIRECTION('',(-1.,0.,0.));
#32431=DIRECTION('center_axis',(1.,0.,0.));
#32432=DIRECTION('ref_axis',(0.,0.,-1.));
#32433=DIRECTION('center_axis',(-1.,0.,0.));
#32434=DIRECTION('ref_axis',(0.,0.,1.));
#32435=DIRECTION('center_axis',(1.,0.,0.));
#32436=DIRECTION('ref_axis',(0.,1.,0.));
#32437=DIRECTION('center_axis',(1.,0.,0.));
#32438=DIRECTION('ref_axis',(0.,0.,-1.));
#32439=DIRECTION('center_axis',(-1.,0.,0.));
#32440=DIRECTION('ref_axis',(0.,1.,0.));
#32441=DIRECTION('center_axis',(1.,0.,0.));
#32442=DIRECTION('ref_axis',(0.,1.,0.));
#32443=DIRECTION('center_axis',(1.,0.,0.));
#32444=DIRECTION('ref_axis',(0.,0.,-1.));
#32445=DIRECTION('',(-1.,0.,0.));
#32446=DIRECTION('center_axis',(1.,0.,0.));
#32447=DIRECTION('ref_axis',(0.,1.,0.));
#32448=DIRECTION('center_axis',(1.,0.,0.));
#32449=DIRECTION('ref_axis',(0.,0.,-1.));
#32450=DIRECTION('',(-1.,0.,0.));
#32451=DIRECTION('center_axis',(1.,0.,0.));
#32452=DIRECTION('ref_axis',(0.,0.,-1.));
#32453=DIRECTION('center_axis',(-1.,0.,0.));
#32454=DIRECTION('ref_axis',(0.,0.,1.));
#32455=DIRECTION('center_axis',(1.,0.,0.));
#32456=DIRECTION('ref_axis',(0.,0.,-1.));
#32457=DIRECTION('center_axis',(1.,0.,0.));
#32458=DIRECTION('ref_axis',(0.,1.,0.));
#32459=DIRECTION('center_axis',(1.,0.,0.));
#32460=DIRECTION('ref_axis',(0.,0.,-1.));
#32461=DIRECTION('',(-1.,0.,0.));
#32462=DIRECTION('center_axis',(1.,0.,0.));
#32463=DIRECTION('ref_axis',(0.,0.,-1.));
#32464=DIRECTION('center_axis',(1.,0.,0.));
#32465=DIRECTION('ref_axis',(0.,0.,-1.));
#32466=DIRECTION('center_axis',(1.,0.,0.));
#32467=DIRECTION('ref_axis',(0.,1.,0.));
#32468=DIRECTION('',(-1.,0.,0.));
#32469=DIRECTION('center_axis',(1.,0.,0.));
#32470=DIRECTION('ref_axis',(0.,0.,-1.));
#32471=DIRECTION('center_axis',(-1.,0.,0.));
#32472=DIRECTION('ref_axis',(0.,0.,1.));
#32473=DIRECTION('center_axis',(1.,0.,0.));
#32474=DIRECTION('ref_axis',(0.,1.,0.));
#32475=DIRECTION('',(-1.,0.,0.));
#32476=DIRECTION('center_axis',(1.,0.,0.));
#32477=DIRECTION('ref_axis',(0.,0.,-1.));
#32478=DIRECTION('center_axis',(1.,0.,0.));
#32479=DIRECTION('ref_axis',(0.,0.,-1.));
#40686=CARTESIAN_POINT('',(0.,0.,0.));
#40687=CARTESIAN_POINT('Origin',(8.,0.,0.));
#40688=CARTESIAN_POINT('',(14.8,-8.5,-1.04094977927525E-15));
#40689=CARTESIAN_POINT('Origin',(14.8,0.,0.));
#40690=CARTESIAN_POINT('',(1.2,-8.5,-1.04094977927525E-15));
#40691=CARTESIAN_POINT('',(8.,-8.5,-1.04094977927525E-15));
#40692=CARTESIAN_POINT('Origin',(1.2,0.,0.));
#40693=CARTESIAN_POINT('Origin',(1.2,10.7,0.));
#40694=CARTESIAN_POINT('',(1.2,-10.7,-1.31037207508767E-15));
#40695=CARTESIAN_POINT('Origin',(1.2,0.,0.));
#40696=CARTESIAN_POINT('Origin',(14.8,8.5,0.));
#40697=CARTESIAN_POINT('',(14.8,-10.7,-1.31037207508767E-15));
#40698=CARTESIAN_POINT('Origin',(14.8,0.,0.));
#40699=CARTESIAN_POINT('Origin',(8.,0.,0.));
#40700=CARTESIAN_POINT('',(15.3,-10.7,-1.31037207508767E-15));
#40701=CARTESIAN_POINT('Origin',(15.3,0.,0.));
#40702=CARTESIAN_POINT('',(8.,-10.7,-1.31037207508767E-15));
#40703=CARTESIAN_POINT('Origin',(0.35,0.,0.));
#40704=CARTESIAN_POINT('',(0.7,-9.,-1.10218211923262E-15));
#40705=CARTESIAN_POINT('Origin',(0.7,0.,0.));
#40706=CARTESIAN_POINT('',(0.,-9.,-1.10218211923262E-15));
#40707=CARTESIAN_POINT('',(0.35,-9.,-1.10218211923262E-15));
#40708=CARTESIAN_POINT('Origin',(0.,0.,0.));
#40709=CARTESIAN_POINT('Origin',(0.,11.5,0.));
#40710=CARTESIAN_POINT('',(0.,-11.5,-1.40834381901946E-15));
#40711=CARTESIAN_POINT('Origin',(0.,0.,0.));
#40712=CARTESIAN_POINT('Origin',(8.,0.,0.));
#40713=CARTESIAN_POINT('',(16.,-11.5,-1.40834381901946E-15));
#40714=CARTESIAN_POINT('Origin',(16.,0.,0.));
#40715=CARTESIAN_POINT('',(8.,-11.5,-1.40834381901946E-15));
#40716=CARTESIAN_POINT('Origin',(16.,9.,0.));
#40717=CARTESIAN_POINT('',(16.,-9.,-1.10218211923262E-15));
#40718=CARTESIAN_POINT('Origin',(16.,0.,0.));
#40719=CARTESIAN_POINT('Origin',(15.65,0.,0.));
#40720=CARTESIAN_POINT('',(15.3,-9.,-1.10218211923262E-15));
#40721=CARTESIAN_POINT('',(15.65,-9.,-1.10218211923262E-15));
#40722=CARTESIAN_POINT('Origin',(15.3,0.,0.));
#40723=CARTESIAN_POINT('Origin',(15.3,10.7,0.));
#40724=CARTESIAN_POINT('Origin',(8.,0.,0.));
#40725=CARTESIAN_POINT('',(0.7,-10.7,-1.31037207508767E-15));
#40726=CARTESIAN_POINT('',(8.,-10.7,-1.31037207508767E-15));
#40727=CARTESIAN_POINT('Origin',(0.7,0.,0.));
#40728=CARTESIAN_POINT('Origin',(0.7,9.,0.));
#46376=UNCERTAINTY_MEASURE_WITH_UNIT(LENGTH_MEASURE(0.01),#46396,
'DISTANCE_ACCURACY_VALUE',
'Maximum model space distance between geometric entities at asserted c
onnectivities');
#46379=UNCERTAINTY_MEASURE_WITH_UNIT(LENGTH_MEASURE(0.01),#46396,
'DISTANCE_ACCURACY_VALUE',
'Maximum model space distance between geometric entities at asserted c
onnectivities');
#46392=(
GEOMETRIC_REPRESENTATION_CONTEXT(3)
GLOBAL_UNCERTAINTY_ASSIGNED_CONTEXT((#46376))
GLOBAL_UNIT_ASSIGNED_CONTEXT((#46396,#46398,#46399))
REPRESENTATION_CONTEXT('','3D')
);
#46395=(
GEOMETRIC_REPRESENTATION_CONTEXT(3)
GLOBAL_UNCERTAINTY_ASSIGNED_CONTEXT((#46379))
GLOBAL_UNIT_ASSIGNED_CONTEXT((#46396,#46398,#46399))
REPRESENTATION_CONTEXT('','3D')
);
#46396=(
LENGTH_UNIT()
NAMED_UNIT(*)
SI_UNIT(.MILLI.,.METRE.)
);
#46398=(
NAMED_UNIT(*)
PLANE_ANGLE_UNIT()
SI_UNIT($,.RADIAN.)
);
#46399=(
NAMED_UNIT(*)
SI_UNIT($,.STERADIAN.)
SOLID_ANGLE_UNIT()
);
#46412=SHAPE_DEFINITION_REPRESENTATION(#46427,#46467);
#46427=PRODUCT_DEFINITION_SHAPE('',$,#46483);
#46467=SHAPE_REPRESENTATION('',(#26580),#46392);
#46470=PRODUCT_DEFINITION_CONTEXT('part definition',#46517,'design');
#46483=PRODUCT_DEFINITION('2026-10-26-00-51-12-008',
'07_Needle_Bearing_HK1716_Drawn_Cup',#46498,#46470);
#46498=PRODUCT_DEFINITION_FORMATION('',$,#46531);
#46517=APPLICATION_CONTEXT(
'Core Data for Automotive Mechanical Design Process');
#46518=PRODUCT_CONTEXT('part definition',#46517,'mechanical');
#46531=PRODUCT('2026-10-26-00-51-12-008',
'07_Needle_Bearing_HK1716_Drawn_Cup',$,(#46518));
#46590=COLOUR_RGB('Grey',0.48,0.52,0.57);
#46591=FILL_AREA_STYLE_COLOUR('',#46590);
#46592=FILL_AREA_STYLE('',(#46591));
#46593=SURFACE_STYLE_FILL_AREA(#46592);
#46594=SURFACE_SIDE_STYLE('',(#46593));
#46595=SURFACE_STYLE_USAGE(.BOTH.,#46594);
#46596=PRESENTATION_STYLE_ASSIGNMENT((#46595));
ENDSEC;
END-ISO-10303-21;
